ISO-10303-21;
HEADER;
FILE_DESCRIPTION (('STEP AP214'),
    '1' );
FILE_NAME ('Part7.step',
    '2026-11-01T05:08:46',
    ( '' ),
    ( '' ),
    'SwSTEP 2.0',
    'SolidWorks 2024',
    '' );
FILE_SCHEMA (( 'AUTOMOTIVE_DESIGN' ));
ENDSEC;

DATA;
#152=CARTESIAN_POINT ( 'NONE',  ( -2.220446049250313081E-13, 135.5000000000000000, 3.000000000000000000 ) ) ;
#319=FACE_OUTER_BOUND ( 'NONE', #3670, .T. ) ;
#363=ADVANCED_FACE ( 'NONE', ( #16549 ), #9863, .F. ) ;
#365=VERTEX_POINT ( 'NONE', #2036 ) ;
#369=ORIENTED_EDGE ( 'NONE', *, *, #6648, .T. ) ;
#429=LINE ( 'NONE', #10904, #12677 ) ;
#435=CARTESIAN_POINT ( 'NONE',  ( -2.216159785453297477E-13, 104.2500000000000142, 3.000000000000000000 ) ) ;
#758=EDGE_CURVE ( 'NONE', #14494, #13306, #7332, .T. ) ;
#899=DIRECTION ( 'NONE',  ( -1.000000000000000000, -0.000000000000000000, -0.000000000000000000 ) ) ;
#979=FACE_OUTER_BOUND ( 'NONE', #10930, .T. ) ;
#980=FACE_OUTER_BOUND ( 'NONE', #7929, .T. ) ;
#1030=DIRECTION ( 'NONE',  ( -0.000000000000000000, 1.000000000000000000, -0.000000000000000000 ) ) ;
#1074=VECTOR ( 'NONE', #899, 1000.000000000000000 ) ;
#1111=CARTESIAN_POINT ( 'NONE',  ( 449.9999999999998295, 75.00000000000001421, 3.000000000000000000 ) ) ;
#1115=PLANE ( 'NONE',  #5608 ) ;
#1260=CARTESIAN_POINT ( 'NONE',  ( 449.9999999999998295, 135.5000000000000000, 3.000000000000000000 ) ) ;
#1289=VECTOR ( 'NONE', #11261, 1000.000000000000000 ) ;
#1335=ORIENTED_EDGE ( 'NONE', *, *, #8749, .F. ) ;
#1362=DIRECTION ( 'NONE',  ( -1.000000000000000000, 0.000000000000000000, 0.000000000000000000 ) ) ;
#1470=ORIENTED_EDGE ( 'NONE', *, *, #15068, .F. ) ;
#1488=AXIS2_PLACEMENT_3D ( 'NONE', #3280, #8693, #15217 ) ;
#1599=CARTESIAN_POINT ( 'NONE',  ( 449.9999999999998295, 135.5000000000000000, 3.000000000000000000 ) ) ;
#1634=EDGE_CURVE ( 'NONE', #13622, #365, #11121, .T. ) ;
#1681=LINE ( 'NONE', #12077, #14454 ) ;
#1734=EDGE_CURVE ( 'NONE', #14532, #4729, #11367, .T. ) ;
#1749=EDGE_LOOP ( 'NONE', ( #3024, #5307, #10350, #1766 ) ) ;
#1760=EDGE_CURVE ( 'NONE', #4729, #13306, #2006, .T. ) ;
#1762=ADVANCED_FACE ( 'NONE', ( #980 ), #3474, .F. ) ;
#1766=ORIENTED_EDGE ( 'NONE', *, *, #8788, .T. ) ;
#1777=DIRECTION ( 'NONE',  ( 0.000000000000000000, 0.000000000000000000, 1.000000000000000000 ) ) ;
#1778=DIRECTION ( 'NONE',  ( -0.000000000000000000, -0.000000000000000000, -1.000000000000000000 ) ) ;
#1782=SURFACE_STYLE_USAGE ( .BOTH. , #13202 ) ;
#1807=ORIENTED_EDGE ( 'NONE', *, *, #1760, .T. ) ;
#1810=PRODUCT ( 'Part7', 'Part7', '', ( #6708 ) ) ;
#1811=DIRECTION ( 'NONE',  ( 1.000000000000000000, 0.000000000000000000, 0.000000000000000000 ) ) ;
#1852=DIRECTION ( 'NONE',  ( 0.000000000000000000, -1.000000000000000000, 0.000000000000000000 ) ) ;
#1859=DIRECTION ( 'NONE',  ( -1.000000000000000000, 0.000000000000000000, 0.000000000000000000 ) ) ;
#1873=DIRECTION ( 'NONE',  ( 0.000000000000000000, -0.000000000000000000, -1.000000000000000000 ) ) ;
#1875=VECTOR ( 'NONE', #7237, 1000.000000000000000 ) ;
#1920=VECTOR ( 'NONE', #1030, 1000.000000000000000 ) ;
#1937=ORIENTED_EDGE ( 'NONE', *, *, #3285, .F. ) ;
#1982=DIRECTION ( 'NONE',  ( 1.000000000000000000, 0.000000000000000000, 0.000000000000000000 ) ) ;
#2006=LINE ( 'NONE', #12747, #1875 ) ;
#2030=PRODUCT_DEFINITION_FORMATION_WITH_SPECIFIED_SOURCE ( 'ANY', '', #1810, .NOT_KNOWN. ) ;
#2036=CARTESIAN_POINT ( 'NONE',  ( -2.220446049250313081E-13, 75.00000000000001421, 3.000000000000000000 ) ) ;
#2058=LINE ( 'NONE', #13833, #5096 ) ;
#2127=ORIENTED_EDGE ( 'NONE', *, *, #2167, .F. ) ;
#2130=EDGE_CURVE ( 'NONE', #14532, #3723, #16651, .T. ) ;
#2150=DIRECTION ( 'NONE',  ( -0.000000000000000000, 0.000000000000000000, 1.000000000000000000 ) ) ;
#2167=EDGE_CURVE ( 'NONE', #365, #8443, #7444, .T. ) ;
#2186=ORIENTED_EDGE ( 'NONE', *, *, #2130, .F. ) ;
#2187=ORIENTED_EDGE ( 'NONE', *, *, #7604, .T. ) ;
#2213=PRODUCT_DEFINITION ( 'UNKNOWN', '', #2030, #16147 ) ;
#2218=CARTESIAN_POINT ( 'NONE',  ( 0.000000000000000000, 0.000000000000000000, 3.000000000000000000 ) ) ;
#2221=SURFACE_STYLE_FILL_AREA ( #3525 ) ;
#2256=LINE ( 'NONE', #4839, #12983 ) ;
#2287=CARTESIAN_POINT ( 'NONE',  ( -2.220446049250313081E-13, 135.5000000000000000, 3.000000000000000000 ) ) ;
#2357=ADVANCED_FACE ( 'NONE', ( #13631 ), #13545, .F. ) ;
#2394=( NAMED_UNIT ( * ) SI_UNIT ( $, .STERADIAN. ) SOLID_ANGLE_UNIT ( ) );
#2462=STYLED_ITEM ( 'NONE', ( #5720 ), #8939 ) ;
#2501=VECTOR ( 'NONE', #1362, 1000.000000000000000 ) ;
#2549=PLANE ( 'NONE',  #6585 ) ;
#2591=VECTOR ( 'NONE', #6590, 1000.000000000000000 ) ;
#2679=EDGE_LOOP ( 'NONE', ( #11434, #1470, #16171, #11259 ) ) ;
#2736=MECHANICAL_DESIGN_GEOMETRIC_PRESENTATION_REPRESENTATION('',(#2462),#7664);
#2756=ORIENTED_EDGE ( 'NONE', *, *, #7691, .F. ) ;
#2823=ORIENTED_EDGE ( 'NONE', *, *, #16958, .T. ) ;
#3024=ORIENTED_EDGE ( 'NONE', *, *, #7892, .T. ) ;
#3062=SURFACE_STYLE_FILL_AREA ( #14832 ) ;
#3136=VERTEX_POINT ( 'NONE', #9969 ) ;
#3153=CARTESIAN_POINT ( 'NONE',  ( -2.220446049250313081E-13, 106.2500000000000142, 0.000000000000000000 ) ) ;
#3183=MANIFOLD_SOLID_BREP ( 'Cut-Extrude1[2]', #5525 ) ;
#3234=DIRECTION ( 'NONE',  ( 1.000000000000000000, 0.000000000000000000, 0.000000000000000000 ) ) ;
#3280=CARTESIAN_POINT ( 'NONE',  ( 0.000000000000000000, 0.000000000000000000, 0.000000000000000000 ) ) ;
#3285=EDGE_CURVE ( 'NONE', #9217, #3723, #8226, .T. ) ;
#3334=DIRECTION ( 'NONE',  ( -1.000000000000000000, 0.000000000000000000, 0.000000000000000000 ) ) ;
#3397=CARTESIAN_POINT ( 'NONE',  ( 0.000000000000000000, 104.2500000000000142, 3.000000000000000000 ) ) ;
#3417=FACE_OUTER_BOUND ( 'NONE', #1749, .T. ) ;
#3426=EDGE_CURVE ( 'NONE', #14494, #13856, #429, .T. ) ;
#3470=ORIENTED_EDGE ( 'NONE', *, *, #8788, .F. ) ;
#3474=PLANE ( 'NONE',  #5149 ) ;
#3524=EDGE_LOOP ( 'NONE', ( #1937, #11015, #2187, #9553 ) ) ;
#3525=FILL_AREA_STYLE ('',( #10054 ) ) ;
#3670=EDGE_LOOP ( 'NONE', ( #1807, #12757, #2186, #8949 ) ) ;
#3715=ADVANCED_FACE ( 'NONE', ( #319 ), #4093, .F. ) ;
#3723=VERTEX_POINT ( 'NONE', #16962 ) ;
#3742=AXIS2_PLACEMENT_3D ( 'NONE', #2218, #15109, #8595 ) ;
#3765=EDGE_LOOP ( 'NONE', ( #10611, #9542, #10668, #10333 ) ) ;
#3794=ORIENTED_EDGE ( 'NONE', *, *, #12603, .T. ) ;
#3840=( GEOMETRIC_REPRESENTATION_CONTEXT ( 3 ) GLOBAL_UNCERTAINTY_ASSIGNED_CONTEXT ( ( #10648 ) ) GLOBAL_UNIT_ASSIGNED_CONTEXT ( ( #7623, #16729, #2394 ) ) REPRESENTATION_CONTEXT ( 'NONE', 'WORKASPACE' ) );
#3953=DIRECTION ( 'NONE',  ( 1.000000000000000000, 0.000000000000000000, 0.000000000000000000 ) ) ;
#3972=( GEOMETRIC_REPRESENTATION_CONTEXT ( 3 ) GLOBAL_UNCERTAINTY_ASSIGNED_CONTEXT ( ( #13971 ) ) GLOBAL_UNIT_ASSIGNED_CONTEXT ( ( #11114, #9830, #10080 ) ) REPRESENTATION_CONTEXT ( 'NONE', 'WORKASPACE' ) );
#4093=PLANE ( 'NONE',  #16018 ) ;
#4177=ADVANCED_FACE ( 'NONE', ( #5496 ), #9642, .F. ) ;
#4339=EDGE_LOOP ( 'NONE', ( #5513, #8062, #7972, #3794 ) ) ;
#4352=ADVANCED_FACE ( 'NONE', ( #15548 ), #1115, .T. ) ;
#4421=LINE ( 'NONE', #9663, #8111 ) ;
#4554=FACE_OUTER_BOUND ( 'NONE', #3524, .T. ) ;
#4649=SHAPE_REPRESENTATION_RELATIONSHIP ( 'NONE' , 'NONE' ,  #15920, #5866 ) ;
#4682=UNCERTAINTY_MEASURE_WITH_UNIT (LENGTH_MEASURE( 1.000000000000000082E-05 ), #11912, 'distance_accuracy_value', 'NONE');
#4729=VERTEX_POINT ( 'NONE', #12441 ) ;
#4806=SURFACE_SIDE_STYLE ('',( #2221 ) ) ;
#4818=ORIENTED_EDGE ( 'NONE', *, *, #7072, .T. ) ;
#4839=CARTESIAN_POINT ( 'NONE',  ( -2.220446049250313081E-13, 75.00000000000001421, 0.000000000000000000 ) ) ;
#5048=CARTESIAN_POINT ( 'NONE',  ( -2.220446049250313081E-13, 135.5000000000000000, 3.000000000000000000 ) ) ;
#5053=CARTESIAN_POINT ( 'NONE',  ( -2.220446049250313081E-13, 75.00000000000001421, 0.000000000000000000 ) ) ;
#5084=CARTESIAN_POINT ( 'NONE',  ( -2.220446049250313081E-13, 75.00000000000001421, 3.000000000000000000 ) ) ;
#5096=VECTOR ( 'NONE', #8760, 1000.000000000000000 ) ;
#5149=AXIS2_PLACEMENT_3D ( 'NONE', #6197, #5959, #15147 ) ;
#5197=FACE_OUTER_BOUND ( 'NONE', #11968, .T. ) ;
#5238=VERTEX_POINT ( 'NONE', #8476 ) ;
#5276=DIRECTION ( 'NONE',  ( -0.000000000000000000, 0.000000000000000000, -1.000000000000000000 ) ) ;
#5280=EDGE_CURVE ( 'NONE', #10097, #13856, #15335, .T. ) ;
#5307=ORIENTED_EDGE ( 'NONE', *, *, #6648, .F. ) ;
#5496=FACE_OUTER_BOUND ( 'NONE', #15207, .T. ) ;
#5513=ORIENTED_EDGE ( 'NONE', *, *, #7892, .F. ) ;
#5525=CLOSED_SHELL ( 'NONE', ( #15595, #4352, #4177, #363, #1762, #12767 ) ) ;
#5587=EDGE_CURVE ( 'NONE', #3136, #5238, #4421, .T. ) ;
#5592=CARTESIAN_POINT ( 'NONE',  ( 0.000000000000000000, 0.000000000000000000, 0.000000000000000000 ) ) ;
#5608=AXIS2_PLACEMENT_3D ( 'NONE', #11675, #10138, #3953 ) ;
#5638=CARTESIAN_POINT ( 'NONE',  ( 449.9999999999998295, 75.00000000000001421, 0.000000000000000000 ) ) ;
#5656=DIRECTION ( 'NONE',  ( -0.000000000000000000, 1.000000000000000000, -0.000000000000000000 ) ) ;
#5720=PRESENTATION_STYLE_ASSIGNMENT (( #1782 ) ) ;
#5796=LINE ( 'NONE', #3397, #8969 ) ;
#5838=PLANE ( 'NONE',  #3742 ) ;
#5851=CARTESIAN_POINT ( 'NONE',  ( 0.000000000000000000, 0.000000000000000000, 0.000000000000000000 ) ) ;
#5866=ADVANCED_BREP_SHAPE_REPRESENTATION ( '', ( #8939, #3183, #1488 ), #3972 ) ;
#5959=DIRECTION ( 'NONE',  ( 1.000000000000000000, 0.000000000000000000, -0.000000000000000000 ) ) ;
#5985=EDGE_LOOP ( 'NONE', ( #1335, #13668, #16117, #15020 ) ) ;
#6007=FACE_OUTER_BOUND ( 'NONE', #3765, .T. ) ;
#6085=ORIENTED_EDGE ( 'NONE', *, *, #8064, .T. ) ;
#6113=PLANE ( 'NONE',  #10258 ) ;
#6197=CARTESIAN_POINT ( 'NONE',  ( -2.220446049250313081E-13, 135.5000000000000000, 3.000000000000000000 ) ) ;
#6229=LINE ( 'NONE', #1260, #12079 ) ;
#6306=DIRECTION ( 'NONE',  ( -0.000000000000000000, -0.000000000000000000, 1.000000000000000000 ) ) ;
#6448=CARTESIAN_POINT ( 'NONE',  ( 449.9999999999998295, 135.5000000000000000, 0.000000000000000000 ) ) ;
#6569=CARTESIAN_POINT ( 'NONE',  ( 449.9999999999998295, 135.5000000000000000, 0.000000000000000000 ) ) ;
#6585=AXIS2_PLACEMENT_3D ( 'NONE', #15688, #13208, #15302 ) ;
#6590=DIRECTION ( 'NONE',  ( -0.000000000000000000, -0.000000000000000000, 1.000000000000000000 ) ) ;
#6648=EDGE_CURVE ( 'NONE', #5238, #11999, #13852, .T. ) ;
#6708=PRODUCT_CONTEXT ( 'NONE', #16199, 'mechanical' ) ;
#7072=EDGE_CURVE ( 'NONE', #3136, #8449, #2058, .T. ) ;
#7084=ADVANCED_FACE ( 'NONE', ( #4554 ), #5838, .T. ) ;
#7237=DIRECTION ( 'NONE',  ( 0.000000000000000000, -1.000000000000000000, 0.000000000000000000 ) ) ;
#7332=LINE ( 'NONE', #15330, #12421 ) ;
#7444=LINE ( 'NONE', #13917, #10656 ) ;
#7479=DIRECTION ( 'NONE',  ( 0.000000000000000000, 1.000000000000000000, 0.000000000000000000 ) ) ;
#7573=LINE ( 'NONE', #6448, #11909 ) ;
#7604=EDGE_CURVE ( 'NONE', #10097, #14532, #14229, .T. ) ;
#7609=ADVANCED_FACE ( 'NONE', ( #14400 ), #16878, .F. ) ;
#7623=( LENGTH_UNIT ( ) NAMED_UNIT ( * ) SI_UNIT ( .MILLI., .METRE. ) );
#7664=( GEOMETRIC_REPRESENTATION_CONTEXT ( 3 ) GLOBAL_UNCERTAINTY_ASSIGNED_CONTEXT ( ( #4682 ) ) GLOBAL_UNIT_ASSIGNED_CONTEXT ( ( #11912, #9334, #8034 ) ) REPRESENTATION_CONTEXT ( 'NONE', 'WORKASPACE' ) );
#7691=EDGE_CURVE ( 'NONE', #8443, #8929, #1681, .T. ) ;
#7892=EDGE_CURVE ( 'NONE', #13622, #11999, #5796, .T. ) ;
#7929=EDGE_LOOP ( 'NONE', ( #12201, #3470, #4818, #9557 ) ) ;
#7940=DIRECTION ( 'NONE',  ( -0.000000000000000000, 1.000000000000000000, 0.000000000000000000 ) ) ;
#7943=AXIS2_PLACEMENT_3D ( 'NONE', #16210, #15266, #1873 ) ;
#7972=ORIENTED_EDGE ( 'NONE', *, *, #2167, .T. ) ;
#7985=DIRECTION ( 'NONE',  ( 1.000000000000000000, 0.000000000000000000, 0.000000000000000000 ) ) ;
#8034=( NAMED_UNIT ( * ) SI_UNIT ( $, .STERADIAN. ) SOLID_ANGLE_UNIT ( ) );
#8062=ORIENTED_EDGE ( 'NONE', *, *, #1634, .T. ) ;
#8064=EDGE_CURVE ( 'NONE', #365, #8449, #11626, .T. ) ;
#8111=VECTOR ( 'NONE', #1811, 1000.000000000000000 ) ;
#8226=LINE ( 'NONE', #13481, #2501 ) ;
#8288=AXIS2_PLACEMENT_3D ( 'NONE', #16633, #3334, #13809 ) ;
#8443=VERTEX_POINT ( 'NONE', #1111 ) ;
#8449=VERTEX_POINT ( 'NONE', #5053 ) ;
#8457=VECTOR ( 'NONE', #16762, 1000.000000000000000 ) ;
#8472=AXIS2_PLACEMENT_3D ( 'NONE', #1599, #1859, #1777 ) ;
#8476=CARTESIAN_POINT ( 'NONE',  ( 449.9999999999998295, 104.2500000000000142, 0.000000000000000000 ) ) ;
#8548=CLOSED_SHELL ( 'NONE', ( #3715, #2357, #7084, #13451, #9540, #7609 ) ) ;
#8595=DIRECTION ( 'NONE',  ( 1.000000000000000000, 0.000000000000000000, 0.000000000000000000 ) ) ;
#8693=DIRECTION ( 'NONE',  ( 0.000000000000000000, 0.000000000000000000, 1.000000000000000000 ) ) ;
#8749=EDGE_CURVE ( 'NONE', #9217, #10097, #6229, .T. ) ;
#8760=DIRECTION ( 'NONE',  ( 0.000000000000000000, -1.000000000000000000, 0.000000000000000000 ) ) ;
#8778=CARTESIAN_POINT ( 'NONE',  ( 449.9999999999998295, 104.2500000000000142, 3.000000000000000000 ) ) ;
#8788=EDGE_CURVE ( 'NONE', #3136, #13622, #10445, .T. ) ;
#8840=DIRECTION ( 'NONE',  ( 0.000000000000000000, -1.000000000000000000, 0.000000000000000000 ) ) ;
#8929=VERTEX_POINT ( 'NONE', #5638 ) ;
#8939=MANIFOLD_SOLID_BREP ( 'Cut-Extrude1[1]', #8548 ) ;
#8949=ORIENTED_EDGE ( 'NONE', *, *, #1734, .T. ) ;
#8969=VECTOR ( 'NONE', #3234, 1000.000000000000000 ) ;
#9061=COLOUR_RGB ( '', 0.09019608, 0.27058824, 0.51372549) ;
#9201=LINE ( 'NONE', #13329, #2591 ) ;
#9217=VERTEX_POINT ( 'NONE', #13360 ) ;
#9291=DIRECTION ( 'NONE',  ( -0.000000000000000000, 0.000000000000000000, 1.000000000000000000 ) ) ;
#9324=ORIENTED_EDGE ( 'NONE', *, *, #7072, .F. ) ;
#9334=( NAMED_UNIT ( * ) PLANE_ANGLE_UNIT ( ) SI_UNIT ( $, .RADIAN. ) );
#9417=DIRECTION ( 'NONE',  ( 0.000000000000000000, -0.000000000000000000, 1.000000000000000000 ) ) ;
#9436=ORIENTED_EDGE ( 'NONE', *, *, #5280, .T. ) ;
#9501=CARTESIAN_POINT ( 'NONE',  ( -2.220446049250313081E-13, 135.5000000000000000, 3.000000000000000000 ) ) ;
#9540=ADVANCED_FACE ( 'NONE', ( #5197 ), #2549, .F. ) ;
#9542=ORIENTED_EDGE ( 'NONE', *, *, #758, .T. ) ;
#9553=ORIENTED_EDGE ( 'NONE', *, *, #2130, .T. ) ;
#9557=ORIENTED_EDGE ( 'NONE', *, *, #8064, .F. ) ;
#9605=ORIENTED_EDGE ( 'NONE', *, *, #12603, .F. ) ;
#9642=PLANE ( 'NONE',  #16584 ) ;
#9663=CARTESIAN_POINT ( 'NONE',  ( -2.216159785453297477E-13, 104.2500000000000142, 0.000000000000000000 ) ) ;
#9830=( NAMED_UNIT ( * ) PLANE_ANGLE_UNIT ( ) SI_UNIT ( $, .RADIAN. ) );
#9863=PLANE ( 'NONE',  #8288 ) ;
#9969=CARTESIAN_POINT ( 'NONE',  ( -2.216159785453297477E-13, 104.2500000000000142, 0.000000000000000000 ) ) ;
#10054=FILL_AREA_STYLE_COLOUR ( '', #9061 ) ;
#10080=( NAMED_UNIT ( * ) SI_UNIT ( $, .STERADIAN. ) SOLID_ANGLE_UNIT ( ) );
#10097=VERTEX_POINT ( 'NONE', #14820 ) ;
#10138=DIRECTION ( 'NONE',  ( -0.000000000000000000, 0.000000000000000000, 1.000000000000000000 ) ) ;
#10167=DIRECTION ( 'NONE',  ( 1.000000000000000000, 0.000000000000000000, 0.000000000000000000 ) ) ;
#10212=DIRECTION ( 'NONE',  ( 1.000000000000000000, 0.000000000000000000, 0.000000000000000000 ) ) ;
#10258=AXIS2_PLACEMENT_3D ( 'NONE', #5084, #7479, #14031 ) ;
#10333=ORIENTED_EDGE ( 'NONE', *, *, #13390, .F. ) ;
#10350=ORIENTED_EDGE ( 'NONE', *, *, #5587, .F. ) ;
#10445=LINE ( 'NONE', #15433, #13166 ) ;
#10590=EDGE_LOOP ( 'NONE', ( #2823, #369, #9605, #15563 ) ) ;
#10611=ORIENTED_EDGE ( 'NONE', *, *, #3426, .F. ) ;
#10644=CARTESIAN_POINT ( 'NONE',  ( -2.220446049250313081E-13, 135.5000000000000000, 3.000000000000000000 ) ) ;
#10648=UNCERTAINTY_MEASURE_WITH_UNIT (LENGTH_MEASURE( 1.000000000000000082E-05 ), #7623, 'distance_accuracy_value', 'NONE');
#10656=VECTOR ( 'NONE', #10212, 1000.000000000000000 ) ;
#10668=ORIENTED_EDGE ( 'NONE', *, *, #1760, .F. ) ;
#10904=CARTESIAN_POINT ( 'NONE',  ( 449.9999999999998295, 135.5000000000000000, 0.000000000000000000 ) ) ;
#10925=VECTOR ( 'NONE', #1852, 1000.000000000000000 ) ;
#10930=EDGE_LOOP ( 'NONE', ( #11719, #2756, #2127, #6085 ) ) ;
#10971=COLOUR_RGB ( '', 0.08235294, 0.09019608, 0.10196078) ;
#11015=ORIENTED_EDGE ( 'NONE', *, *, #8749, .T. ) ;
#11085=ORIENTED_EDGE ( 'NONE', *, *, #16958, .F. ) ;
#11114=( LENGTH_UNIT ( ) NAMED_UNIT ( * ) SI_UNIT ( .MILLI., .METRE. ) );
#11121=LINE ( 'NONE', #9501, #10925 ) ;
#11259=ORIENTED_EDGE ( 'NONE', *, *, #16229, .T. ) ;
#11261=DIRECTION ( 'NONE',  ( -0.000000000000000000, -0.000000000000000000, 1.000000000000000000 ) ) ;
#11367=LINE ( 'NONE', #11530, #8457 ) ;
#11421=PRESENTATION_STYLE_ASSIGNMENT (( #15294 ) ) ;
#11434=ORIENTED_EDGE ( 'NONE', *, *, #3285, .T. ) ;
#11477=EDGE_CURVE ( 'NONE', #8449, #8929, #2256, .T. ) ;
#11530=CARTESIAN_POINT ( 'NONE',  ( -2.220446049250313081E-13, 135.5000000000000000, 3.000000000000000000 ) ) ;
#11531=DIRECTION ( 'NONE',  ( -0.000000000000000000, 1.000000000000000000, -0.000000000000000000 ) ) ;
#11532=LINE ( 'NONE', #12658, #1074 ) ;
#11536=DIRECTION ( 'NONE',  ( -1.000000000000000000, -0.000000000000000000, -0.000000000000000000 ) ) ;
#11626=LINE ( 'NONE', #14287, #13910 ) ;
#11675=CARTESIAN_POINT ( 'NONE',  ( 0.000000000000000000, 0.000000000000000000, 3.000000000000000000 ) ) ;
#11719=ORIENTED_EDGE ( 'NONE', *, *, #11477, .T. ) ;
#11909=VECTOR ( 'NONE', #11531, 1000.000000000000000 ) ;
#11912=( LENGTH_UNIT ( ) NAMED_UNIT ( * ) SI_UNIT ( .MILLI., .METRE. ) );
#11968=EDGE_LOOP ( 'NONE', ( #14200, #14212, #16777, #9436 ) ) ;
#11978=VECTOR ( 'NONE', #15522, 1000.000000000000000 ) ;
#11999=VERTEX_POINT ( 'NONE', #8778 ) ;
#12024=CARTESIAN_POINT ( 'NONE',  ( 449.9999999999998295, 106.2500000000000142, 0.000000000000000000 ) ) ;
#12077=CARTESIAN_POINT ( 'NONE',  ( 449.9999999999998295, 75.00000000000001421, 3.000000000000000000 ) ) ;
#12079=VECTOR ( 'NONE', #16712, 1000.000000000000000 ) ;
#12201=ORIENTED_EDGE ( 'NONE', *, *, #1634, .F. ) ;
#12232=PRODUCT_DEFINITION_SHAPE ( 'NONE', 'NONE',  #2213 ) ;
#12337=AXIS2_PLACEMENT_3D ( 'NONE', #5851, #2150, #1982 ) ;
#12343=CARTESIAN_POINT ( 'NONE',  ( -2.216159785453297477E-13, 106.2500000000000142, 0.000000000000000000 ) ) ;
#12421=VECTOR ( 'NONE', #11536, 1000.000000000000000 ) ;
#12441=CARTESIAN_POINT ( 'NONE',  ( -2.220446049250313081E-13, 135.5000000000000000, 0.000000000000000000 ) ) ;
#12603=EDGE_CURVE ( 'NONE', #8443, #11999, #16725, .T. ) ;
#12658=CARTESIAN_POINT ( 'NONE',  ( -2.220446049250313081E-13, 135.5000000000000000, 0.000000000000000000 ) ) ;
#12677=VECTOR ( 'NONE', #5656, 1000.000000000000000 ) ;
#12747=CARTESIAN_POINT ( 'NONE',  ( -2.220446049250313081E-13, 135.5000000000000000, 0.000000000000000000 ) ) ;
#12753=DIRECTION ( 'NONE',  ( -0.000000000000000000, -0.000000000000000000, -1.000000000000000000 ) ) ;
#12757=ORIENTED_EDGE ( 'NONE', *, *, #15068, .T. ) ;
#12767=ADVANCED_FACE ( 'NONE', ( #3417 ), #13649, .F. ) ;
#12868=CARTESIAN_POINT ( 'NONE',  ( 449.9999999999998295, 135.5000000000000000, 3.000000000000000000 ) ) ;
#12983=VECTOR ( 'NONE', #10167, 1000.000000000000000 ) ;
#13077=ORIENTED_EDGE ( 'NONE', *, *, #11477, .F. ) ;
#13116=DIRECTION ( 'NONE',  ( 1.000000000000000000, 0.000000000000000000, -0.000000000000000000 ) ) ;
#13166=VECTOR ( 'NONE', #6306, 1000.000000000000000 ) ;
#13202=SURFACE_SIDE_STYLE ('',( #3062 ) ) ;
#13208=DIRECTION ( 'NONE',  ( 0.000000000000000000, -1.000000000000000000, 0.000000000000000000 ) ) ;
#13306=VERTEX_POINT ( 'NONE', #3153 ) ;
#13329=CARTESIAN_POINT ( 'NONE',  ( 449.9999999999998295, 106.2500000000000142, 0.000000000000000000 ) ) ;
#13360=CARTESIAN_POINT ( 'NONE',  ( 449.9999999999998295, 106.2500000000000142, 3.000000000000000000 ) ) ;
#13390=EDGE_CURVE ( 'NONE', #13856, #4729, #11532, .T. ) ;
#13451=ADVANCED_FACE ( 'NONE', ( #6007 ), #13753, .F. ) ;
#13481=CARTESIAN_POINT ( 'NONE',  ( 0.000000000000000000, 106.2500000000000142, 3.000000000000000000 ) ) ;
#13545=PLANE ( 'NONE',  #8472 ) ;
#13546=CARTESIAN_POINT ( 'NONE',  ( -2.216159785453297477E-13, 106.2500000000000142, 0.000000000000000000 ) ) ;
#13606=VECTOR ( 'NONE', #15582, 1000.000000000000000 ) ;
#13622=VERTEX_POINT ( 'NONE', #435 ) ;
#13631=FACE_OUTER_BOUND ( 'NONE', #5985, .T. ) ;
#13645=LINE ( 'NONE', #12343, #14906 ) ;
#13649=PLANE ( 'NONE',  #7943 ) ;
#13668=ORIENTED_EDGE ( 'NONE', *, *, #16229, .F. ) ;
#13753=PLANE ( 'NONE',  #12337 ) ;
#13799=DIRECTION ( 'NONE',  ( -0.000000000000000000, -0.000000000000000000, 1.000000000000000000 ) ) ;
#13809=DIRECTION ( 'NONE',  ( 0.000000000000000000, 0.000000000000000000, 1.000000000000000000 ) ) ;
#13833=CARTESIAN_POINT ( 'NONE',  ( -2.220446049250313081E-13, 135.5000000000000000, 0.000000000000000000 ) ) ;
#13852=LINE ( 'NONE', #16419, #1289 ) ;
#13856=VERTEX_POINT ( 'NONE', #6569 ) ;
#13910=VECTOR ( 'NONE', #12753, 1000.000000000000000 ) ;
#13917=CARTESIAN_POINT ( 'NONE',  ( -2.220446049250313081E-13, 75.00000000000001421, 3.000000000000000000 ) ) ;
#13971=UNCERTAINTY_MEASURE_WITH_UNIT (LENGTH_MEASURE( 1.000000000000000082E-05 ), #11114, 'distance_accuracy_value', 'NONE');
#14031=DIRECTION ( 'NONE',  ( 0.000000000000000000, -0.000000000000000000, 1.000000000000000000 ) ) ;
#14200=ORIENTED_EDGE ( 'NONE', *, *, #13390, .T. ) ;
#14212=ORIENTED_EDGE ( 'NONE', *, *, #1734, .F. ) ;
#14229=LINE ( 'NONE', #2287, #11978 ) ;
#14287=CARTESIAN_POINT ( 'NONE',  ( -2.220446049250313081E-13, 75.00000000000001421, 3.000000000000000000 ) ) ;
#14400=FACE_OUTER_BOUND ( 'NONE', #2679, .T. ) ;
#14454=VECTOR ( 'NONE', #1778, 1000.000000000000000 ) ;
#14494=VERTEX_POINT ( 'NONE', #12024 ) ;
#14532=VERTEX_POINT ( 'NONE', #10644 ) ;
#14543=STYLED_ITEM ( 'NONE', ( #11421 ), #3183 ) ;
#14729=AXIS2_PLACEMENT_3D ( 'NONE', #13546, #7940, #9417 ) ;
#14798=SHAPE_DEFINITION_REPRESENTATION ( #12232, #15920 ) ;
#14820=CARTESIAN_POINT ( 'NONE',  ( 449.9999999999998295, 135.5000000000000000, 3.000000000000000000 ) ) ;
#14832=FILL_AREA_STYLE ('',( #14914 ) ) ;
#14845=ORIENTED_EDGE ( 'NONE', *, *, #5587, .T. ) ;
#14906=VECTOR ( 'NONE', #13799, 1000.000000000000000 ) ;
#14914=FILL_AREA_STYLE_COLOUR ( '', #10971 ) ;
#15020=ORIENTED_EDGE ( 'NONE', *, *, #5280, .F. ) ;
#15068=EDGE_CURVE ( 'NONE', #13306, #3723, #13645, .T. ) ;
#15109=DIRECTION ( 'NONE',  ( -0.000000000000000000, 0.000000000000000000, 1.000000000000000000 ) ) ;
#15147=DIRECTION ( 'NONE',  ( -0.000000000000000000, 0.000000000000000000, -1.000000000000000000 ) ) ;
#15207=EDGE_LOOP ( 'NONE', ( #9324, #14845, #11085, #13077 ) ) ;
#15217=DIRECTION ( 'NONE',  ( 1.000000000000000000, 0.000000000000000000, 0.000000000000000000 ) ) ;
#15266=DIRECTION ( 'NONE',  ( 0.000000000000000000, -1.000000000000000000, 0.000000000000000000 ) ) ;
#15294=SURFACE_STYLE_USAGE ( .BOTH. , #4806 ) ;
#15302=DIRECTION ( 'NONE',  ( 0.000000000000000000, -0.000000000000000000, -1.000000000000000000 ) ) ;
#15330=CARTESIAN_POINT ( 'NONE',  ( -2.216159785453297477E-13, 106.2500000000000142, 0.000000000000000000 ) ) ;
#15335=LINE ( 'NONE', #15415, #13606 ) ;
#15415=CARTESIAN_POINT ( 'NONE',  ( 449.9999999999998295, 135.5000000000000000, 3.000000000000000000 ) ) ;
#15433=CARTESIAN_POINT ( 'NONE',  ( -2.216159785453297477E-13, 104.2500000000000142, 0.000000000000000000 ) ) ;
#15522=DIRECTION ( 'NONE',  ( -1.000000000000000000, -0.000000000000000000, -0.000000000000000000 ) ) ;
#15548=FACE_OUTER_BOUND ( 'NONE', #4339, .T. ) ;
#15549=APPLICATION_CONTEXT ( 'automotive_design' ) ;
#15563=ORIENTED_EDGE ( 'NONE', *, *, #7691, .T. ) ;
#15582=DIRECTION ( 'NONE',  ( -0.000000000000000000, -0.000000000000000000, -1.000000000000000000 ) ) ;
#15595=ADVANCED_FACE ( 'NONE', ( #979 ), #6113, .F. ) ;
#15688=CARTESIAN_POINT ( 'NONE',  ( -2.220446049250313081E-13, 135.5000000000000000, 3.000000000000000000 ) ) ;
#15920=SHAPE_REPRESENTATION ( 'Part7', ( #1488 ), #3972 ) ;
#16018=AXIS2_PLACEMENT_3D ( 'NONE', #152, #13116, #5276 ) ;
#16117=ORIENTED_EDGE ( 'NONE', *, *, #3426, .T. ) ;
#16147=PRODUCT_DEFINITION_CONTEXT ( 'detailed design', #15549, 'design' ) ;
#16171=ORIENTED_EDGE ( 'NONE', *, *, #758, .F. ) ;
#16185=MECHANICAL_DESIGN_GEOMETRIC_PRESENTATION_REPRESENTATION('',(#14543),#3840);
#16199=APPLICATION_CONTEXT ( 'automotive_design' ) ;
#16210=CARTESIAN_POINT ( 'NONE',  ( -2.216159785453297477E-13, 104.2500000000000142, 0.000000000000000000 ) ) ;
#16229=EDGE_CURVE ( 'NONE', #14494, #9217, #9201, .T. ) ;
#16419=CARTESIAN_POINT ( 'NONE',  ( 449.9999999999998295, 104.2500000000000142, 0.000000000000000000 ) ) ;
#16549=FACE_OUTER_BOUND ( 'NONE', #10590, .T. ) ;
#16584=AXIS2_PLACEMENT_3D ( 'NONE', #5592, #9291, #7985 ) ;
#16633=CARTESIAN_POINT ( 'NONE',  ( 449.9999999999998295, 135.5000000000000000, 3.000000000000000000 ) ) ;
#16651=LINE ( 'NONE', #5048, #16677 ) ;
#16677=VECTOR ( 'NONE', #8840, 1000.000000000000000 ) ;
#16712=DIRECTION ( 'NONE',  ( -0.000000000000000000, 1.000000000000000000, -0.000000000000000000 ) ) ;
#16725=LINE ( 'NONE', #12868, #1920 ) ;
#16729=( NAMED_UNIT ( * ) PLANE_ANGLE_UNIT ( ) SI_UNIT ( $, .RADIAN. ) );
#16762=DIRECTION ( 'NONE',  ( -0.000000000000000000, -0.000000000000000000, -1.000000000000000000 ) ) ;
#16777=ORIENTED_EDGE ( 'NONE', *, *, #7604, .F. ) ;
#16878=PLANE ( 'NONE',  #14729 ) ;
#16958=EDGE_CURVE ( 'NONE', #8929, #5238, #7573, .T. ) ;
#16962=CARTESIAN_POINT ( 'NONE',  ( -2.216159785453297477E-13, 106.2500000000000142, 3.000000000000000000 ) ) ;
ENDSEC;
END-ISO-10303-21;
